ISO-10303-21;
HEADER;
/* Generated by software containing ST-Developer
 * from STEP Tools, Inc. (www.steptools.com) 
 */

FILE_DESCRIPTION(
/* description */ ('Flywheel Crank-Slider'),
/* implementation_level */ '2;1');

FILE_NAME(
/* name */ 'M8x25 Bolt.step',
/* time_stamp */ '2026-10-28T03:23:13-07:00',
/* author */ (''),
/* organization */ (''),
/* preprocessor_version */ 'ST-DEVELOPER v20.2',
/* originating_system */ 'Autodesk Translation Framework v15.17.0.0',
/* authorisation */ '');

FILE_SCHEMA (('AUTOMOTIVE_DESIGN { 1 0 10303 214 3 1 1 }'));
ENDSEC;

DATA;
#10=MECHANICAL_DESIGN_GEOMETRIC_PRESENTATION_REPRESENTATION('',(#684),#17322);
#530=ORIENTED_CLOSED_SHELL('',*,#9063,.F.);
#538=CONICAL_SURFACE('',#10066,0.625,0.785398163397448);
#539=CONICAL_SURFACE('',#10070,0.635,0.785398163397449);
#540=CONICAL_SURFACE('',#10074,0.41,0.463647609000806);
#560=BREP_WITH_VOIDS('Body1',#9064,(#530));
#579=SHAPE_REPRESENTATION_RELATIONSHIP('SRR','None',#17576,#631);
#631=ADVANCED_BREP_SHAPE_REPRESENTATION('',(#560),#17280);
#684=STYLED_ITEM('',(#17938),#560);
#893=FACE_BOUND('',#2171,.T.);
#1122=PLANE('',#10054);
#1123=PLANE('',#10055);
#1124=PLANE('',#10056);
#1125=PLANE('',#10057);
#1126=PLANE('',#10058);
#1127=PLANE('',#10059);
#1128=PLANE('',#10060);
#1129=PLANE('',#10061);
#1130=PLANE('',#10062);
#1131=PLANE('',#10064);
#1132=PLANE('',#10072);
#1514=FACE_OUTER_BOUND('',#2157,.T.);
#1515=FACE_OUTER_BOUND('',#2158,.T.);
#1516=FACE_OUTER_BOUND('',#2159,.T.);
#1517=FACE_OUTER_BOUND('',#2160,.T.);
#1518=FACE_OUTER_BOUND('',#2161,.T.);
#1519=FACE_OUTER_BOUND('',#2162,.T.);
#1520=FACE_OUTER_BOUND('',#2163,.T.);
#1521=FACE_OUTER_BOUND('',#2164,.T.);
#1522=FACE_OUTER_BOUND('',#2165,.T.);
#1523=FACE_OUTER_BOUND('',#2166,.T.);
#1524=FACE_OUTER_BOUND('',#2167,.T.);
#1525=FACE_OUTER_BOUND('',#2168,.T.);
#1526=FACE_OUTER_BOUND('',#2169,.T.);
#1527=FACE_OUTER_BOUND('',#2170,.T.);
#1528=FACE_OUTER_BOUND('',#2172,.T.);
#1529=FACE_OUTER_BOUND('',#2173,.T.);
#2157=EDGE_LOOP('',(#6942,#6943,#6944,#6945));
#2158=EDGE_LOOP('',(#6946,#6947,#6948,#6949));
#2159=EDGE_LOOP('',(#6950,#6951,#6952,#6953));
#2160=EDGE_LOOP('',(#6954,#6955,#6956,#6957));
#2161=EDGE_LOOP('',(#6958,#6959,#6960,#6961));
#2162=EDGE_LOOP('',(#6962,#6963,#6964,#6965));
#2163=EDGE_LOOP('',(#6966,#6967,#6968,#6969,#6970,#6971));
#2164=EDGE_LOOP('',(#6972,#6973,#6974,#6975,#6976,#6977));
#2165=EDGE_LOOP('',(#6978));
#2166=EDGE_LOOP('',(#6979));
#2167=EDGE_LOOP('',(#6980,#6981,#6982,#6983));
#2168=EDGE_LOOP('',(#6984,#6985,#6986,#6987));
#2169=EDGE_LOOP('',(#6988,#6989,#6990,#6991));
#2170=EDGE_LOOP('',(#6992));
#2171=EDGE_LOOP('',(#6993));
#2172=EDGE_LOOP('',(#6994,#6995,#6996,#6997));
#2173=EDGE_LOOP('',(#6998,#6999,#7000,#7001));
#2848=LINE('',#15041,#3459);
#2849=LINE('',#15043,#3460);
#2850=LINE('',#15045,#3461);
#2851=LINE('',#15046,#3462);
#2852=LINE('',#15049,#3463);
#2853=LINE('',#15051,#3464);
#2854=LINE('',#15052,#3465);
#2855=LINE('',#15055,#3466);
#2856=LINE('',#15057,#3467);
#2857=LINE('',#15058,#3468);
#2858=LINE('',#15061,#3469);
#2859=LINE('',#15063,#3470);
#2860=LINE('',#15064,#3471);
#2861=LINE('',#15067,#3472);
#2862=LINE('',#15069,#3473);
#2863=LINE('',#15070,#3474);
#2864=LINE('',#15072,#3475);
#2865=LINE('',#15073,#3476);
#2866=LINE('',#15085,#3477);
#2867=LINE('',#15089,#3478);
#2868=LINE('',#15093,#3479);
#2869=LINE('',#15100,#3480);
#2870=LINE('',#15102,#3481);
#3459=VECTOR('',#11802,1.);
#3460=VECTOR('',#11803,1.);
#3461=VECTOR('',#11804,1.);
#3462=VECTOR('',#11805,1.);
#3463=VECTOR('',#11808,1.);
#3464=VECTOR('',#11809,1.);
#3465=VECTOR('',#11810,1.);
#3466=VECTOR('',#11813,1.);
#3467=VECTOR('',#11814,1.);
#3468=VECTOR('',#11815,1.);
#3469=VECTOR('',#11818,1.);
#3470=VECTOR('',#11819,1.);
#3471=VECTOR('',#11820,1.);
#3472=VECTOR('',#11823,1.);
#3473=VECTOR('',#11824,1.);
#3474=VECTOR('',#11825,1.);
#3475=VECTOR('',#11828,1.);
#3476=VECTOR('',#11829,1.);
#3477=VECTOR('',#11846,0.625);
#3478=VECTOR('',#11851,0.65);
#3479=VECTOR('',#11856,0.635);
#3480=VECTOR('',#11865,0.41);
#3481=VECTOR('',#11868,0.4);
#3992=CIRCLE('',#10063,0.3933);
#3993=CIRCLE('',#10065,0.6);
#3994=CIRCLE('',#10067,0.65);
#3995=CIRCLE('',#10069,0.65);
#3996=CIRCLE('',#10071,0.62);
#3997=CIRCLE('',#10073,0.42);
#3998=CIRCLE('',#10075,0.3933);
#4551=VERTEX_POINT('',#15039);
#4552=VERTEX_POINT('',#15040);
#4553=VERTEX_POINT('',#15042);
#4554=VERTEX_POINT('',#15044);
#4555=VERTEX_POINT('',#15048);
#4556=VERTEX_POINT('',#15050);
#4557=VERTEX_POINT('',#15054);
#4558=VERTEX_POINT('',#15056);
#4559=VERTEX_POINT('',#15060);
#4560=VERTEX_POINT('',#15062);
#4561=VERTEX_POINT('',#15066);
#4562=VERTEX_POINT('',#15068);
#4563=VERTEX_POINT('',#15077);
#4564=VERTEX_POINT('',#15080);
#4565=VERTEX_POINT('',#15083);
#4566=VERTEX_POINT('',#15087);
#4567=VERTEX_POINT('',#15091);
#4568=VERTEX_POINT('',#15095);
#4569=VERTEX_POINT('',#15098);
#5428=EDGE_CURVE('',#4551,#4552,#2848,.T.);
#5429=EDGE_CURVE('',#4552,#4553,#2849,.T.);
#5430=EDGE_CURVE('',#4553,#4554,#2850,.T.);
#5431=EDGE_CURVE('',#4551,#4554,#2851,.T.);
#5432=EDGE_CURVE('',#4552,#4555,#2852,.T.);
#5433=EDGE_CURVE('',#4555,#4556,#2853,.T.);
#5434=EDGE_CURVE('',#4556,#4553,#2854,.T.);
#5435=EDGE_CURVE('',#4555,#4557,#2855,.T.);
#5436=EDGE_CURVE('',#4557,#4558,#2856,.T.);
#5437=EDGE_CURVE('',#4558,#4556,#2857,.T.);
#5438=EDGE_CURVE('',#4557,#4559,#2858,.T.);
#5439=EDGE_CURVE('',#4559,#4560,#2859,.T.);
#5440=EDGE_CURVE('',#4560,#4558,#2860,.T.);
#5441=EDGE_CURVE('',#4559,#4561,#2861,.T.);
#5442=EDGE_CURVE('',#4561,#4562,#2862,.T.);
#5443=EDGE_CURVE('',#4562,#4560,#2863,.T.);
#5444=EDGE_CURVE('',#4561,#4551,#2864,.T.);
#5445=EDGE_CURVE('',#4554,#4562,#2865,.T.);
#5446=EDGE_CURVE('',#4563,#4563,#3992,.T.);
#5447=EDGE_CURVE('',#4564,#4564,#3993,.T.);
#5448=EDGE_CURVE('',#4565,#4565,#3994,.T.);
#5449=EDGE_CURVE('',#4565,#4564,#2866,.T.);
#5450=EDGE_CURVE('',#4566,#4566,#3995,.T.);
#5451=EDGE_CURVE('',#4566,#4565,#2867,.T.);
#5452=EDGE_CURVE('',#4567,#4567,#3996,.T.);
#5453=EDGE_CURVE('',#4567,#4566,#2868,.T.);
#5454=EDGE_CURVE('',#4568,#4568,#3997,.T.);
#5455=EDGE_CURVE('',#4569,#4569,#3998,.F.);
#5456=EDGE_CURVE('',#4569,#4568,#2869,.T.);
#5457=EDGE_CURVE('',#4563,#4569,#2870,.T.);
#6942=ORIENTED_EDGE('',*,*,#5428,.T.);
#6943=ORIENTED_EDGE('',*,*,#5429,.T.);
#6944=ORIENTED_EDGE('',*,*,#5430,.T.);
#6945=ORIENTED_EDGE('',*,*,#5431,.F.);
#6946=ORIENTED_EDGE('',*,*,#5432,.T.);
#6947=ORIENTED_EDGE('',*,*,#5433,.T.);
#6948=ORIENTED_EDGE('',*,*,#5434,.T.);
#6949=ORIENTED_EDGE('',*,*,#5429,.F.);
#6950=ORIENTED_EDGE('',*,*,#5435,.T.);
#6951=ORIENTED_EDGE('',*,*,#5436,.T.);
#6952=ORIENTED_EDGE('',*,*,#5437,.T.);
#6953=ORIENTED_EDGE('',*,*,#5433,.F.);
#6954=ORIENTED_EDGE('',*,*,#5438,.T.);
#6955=ORIENTED_EDGE('',*,*,#5439,.T.);
#6956=ORIENTED_EDGE('',*,*,#5440,.T.);
#6957=ORIENTED_EDGE('',*,*,#5436,.F.);
#6958=ORIENTED_EDGE('',*,*,#5441,.T.);
#6959=ORIENTED_EDGE('',*,*,#5442,.T.);
#6960=ORIENTED_EDGE('',*,*,#5443,.T.);
#6961=ORIENTED_EDGE('',*,*,#5439,.F.);
#6962=ORIENTED_EDGE('',*,*,#5444,.T.);
#6963=ORIENTED_EDGE('',*,*,#5431,.T.);
#6964=ORIENTED_EDGE('',*,*,#5445,.T.);
#6965=ORIENTED_EDGE('',*,*,#5442,.F.);
#6966=ORIENTED_EDGE('',*,*,#5444,.F.);
#6967=ORIENTED_EDGE('',*,*,#5441,.F.);
#6968=ORIENTED_EDGE('',*,*,#5438,.F.);
#6969=ORIENTED_EDGE('',*,*,#5435,.F.);
#6970=ORIENTED_EDGE('',*,*,#5432,.F.);
#6971=ORIENTED_EDGE('',*,*,#5428,.F.);
#6972=ORIENTED_EDGE('',*,*,#5445,.F.);
#6973=ORIENTED_EDGE('',*,*,#5430,.F.);
#6974=ORIENTED_EDGE('',*,*,#5434,.F.);
#6975=ORIENTED_EDGE('',*,*,#5437,.F.);
#6976=ORIENTED_EDGE('',*,*,#5440,.F.);
#6977=ORIENTED_EDGE('',*,*,#5443,.F.);
#6978=ORIENTED_EDGE('',*,*,#5446,.F.);
#6979=ORIENTED_EDGE('',*,*,#5447,.F.);
#6980=ORIENTED_EDGE('',*,*,#5448,.F.);
#6981=ORIENTED_EDGE('',*,*,#5449,.T.);
#6982=ORIENTED_EDGE('',*,*,#5447,.T.);
#6983=ORIENTED_EDGE('',*,*,#5449,.F.);
#6984=ORIENTED_EDGE('',*,*,#5450,.F.);
#6985=ORIENTED_EDGE('',*,*,#5451,.T.);
#6986=ORIENTED_EDGE('',*,*,#5448,.T.);
#6987=ORIENTED_EDGE('',*,*,#5451,.F.);
#6988=ORIENTED_EDGE('',*,*,#5452,.F.);
#6989=ORIENTED_EDGE('',*,*,#5453,.T.);
#6990=ORIENTED_EDGE('',*,*,#5450,.T.);
#6991=ORIENTED_EDGE('',*,*,#5453,.F.);
#6992=ORIENTED_EDGE('',*,*,#5452,.T.);
#6993=ORIENTED_EDGE('',*,*,#5454,.F.);
#6994=ORIENTED_EDGE('',*,*,#5455,.F.);
#6995=ORIENTED_EDGE('',*,*,#5456,.T.);
#6996=ORIENTED_EDGE('',*,*,#5454,.T.);
#6997=ORIENTED_EDGE('',*,*,#5456,.F.);
#6998=ORIENTED_EDGE('',*,*,#5446,.T.);
#6999=ORIENTED_EDGE('',*,*,#5457,.T.);
#7000=ORIENTED_EDGE('',*,*,#5455,.T.);
#7001=ORIENTED_EDGE('',*,*,#5457,.F.);
#8407=CYLINDRICAL_SURFACE('',#10068,0.65);
#8408=CYLINDRICAL_SURFACE('',#10076,0.3933);
#8705=ADVANCED_FACE('',(#1514),#1122,.F.);
#8706=ADVANCED_FACE('',(#1515),#1123,.F.);
#8707=ADVANCED_FACE('',(#1516),#1124,.F.);
#8708=ADVANCED_FACE('',(#1517),#1125,.F.);
#8709=ADVANCED_FACE('',(#1518),#1126,.F.);
#8710=ADVANCED_FACE('',(#1519),#1127,.F.);
#8711=ADVANCED_FACE('',(#1520),#1128,.F.);
#8712=ADVANCED_FACE('',(#1521),#1129,.F.);
#8713=ADVANCED_FACE('',(#1522),#1130,.F.);
#8714=ADVANCED_FACE('',(#1523),#1131,.T.);
#8715=ADVANCED_FACE('',(#1524),#538,.T.);
#8716=ADVANCED_FACE('',(#1525),#8407,.T.);
#8717=ADVANCED_FACE('',(#1526),#539,.T.);
#8718=ADVANCED_FACE('',(#1527,#893),#1132,.T.);
#8719=ADVANCED_FACE('',(#1528),#540,.T.);
#8720=ADVANCED_FACE('',(#1529),#8408,.T.);
#9063=CLOSED_SHELL('',(#8705,#8706,#8707,#8708,#8709,#8710,#8711,#8712));
#9064=CLOSED_SHELL('',(#8713,#8714,#8715,#8716,#8717,#8718,#8719,#8720));
#10053=AXIS2_PLACEMENT_3D('',#15037,#11798,#11799);
#10054=AXIS2_PLACEMENT_3D('',#15038,#11800,#11801);
#10055=AXIS2_PLACEMENT_3D('',#15047,#11806,#11807);
#10056=AXIS2_PLACEMENT_3D('',#15053,#11811,#11812);
#10057=AXIS2_PLACEMENT_3D('',#15059,#11816,#11817);
#10058=AXIS2_PLACEMENT_3D('',#15065,#11821,#11822);
#10059=AXIS2_PLACEMENT_3D('',#15071,#11826,#11827);
#10060=AXIS2_PLACEMENT_3D('',#15074,#11830,#11831);
#10061=AXIS2_PLACEMENT_3D('',#15075,#11832,#11833);
#10062=AXIS2_PLACEMENT_3D('',#15076,#11834,#11835);
#10063=AXIS2_PLACEMENT_3D('',#15078,#11836,#11837);
#10064=AXIS2_PLACEMENT_3D('',#15079,#11838,#11839);
#10065=AXIS2_PLACEMENT_3D('',#15081,#11840,#11841);
#10066=AXIS2_PLACEMENT_3D('',#15082,#11842,#11843);
#10067=AXIS2_PLACEMENT_3D('',#15084,#11844,#11845);
#10068=AXIS2_PLACEMENT_3D('',#15086,#11847,#11848);
#10069=AXIS2_PLACEMENT_3D('',#15088,#11849,#11850);
#10070=AXIS2_PLACEMENT_3D('',#15090,#11852,#11853);
#10071=AXIS2_PLACEMENT_3D('',#15092,#11854,#11855);
#10072=AXIS2_PLACEMENT_3D('',#15094,#11857,#11858);
#10073=AXIS2_PLACEMENT_3D('',#15096,#11859,#11860);
#10074=AXIS2_PLACEMENT_3D('',#15097,#11861,#11862);
#10075=AXIS2_PLACEMENT_3D('',#15099,#11863,#11864);
#10076=AXIS2_PLACEMENT_3D('',#15101,#11866,#11867);
#11798=DIRECTION('axis',(0.,0.,1.));
#11799=DIRECTION('refdir',(1.,0.,0.));
#11800=DIRECTION('center_axis',(0.866025403784439,0.,-0.5));
#11801=DIRECTION('ref_axis',(0.5,0.,0.866025403784439));
#11802=DIRECTION('',(-0.5,0.,-0.866025403784439));
#11803=DIRECTION('',(0.,-1.,0.));
#11804=DIRECTION('',(0.5,0.,0.866025403784439));
#11805=DIRECTION('',(0.,-1.,0.));
#11806=DIRECTION('center_axis',(1.60246890531964E-16,0.,-1.));
#11807=DIRECTION('ref_axis',(1.,0.,1.60246890531964E-16));
#11808=DIRECTION('',(-1.,0.,-1.60246890531964E-16));
#11809=DIRECTION('',(0.,-1.,0.));
#11810=DIRECTION('',(1.,0.,1.60246890531964E-16));
#11811=DIRECTION('center_axis',(-0.866025403784439,0.,-0.5));
#11812=DIRECTION('ref_axis',(0.5,0.,-0.866025403784439));
#11813=DIRECTION('',(-0.5,0.,0.866025403784439));
#11814=DIRECTION('',(0.,-1.,0.));
#11815=DIRECTION('',(0.5,0.,-0.866025403784439));
#11816=DIRECTION('center_axis',(-0.866025403784439,0.,0.5));
#11817=DIRECTION('ref_axis',(-0.5,0.,-0.866025403784439));
#11818=DIRECTION('',(0.5,0.,0.866025403784439));
#11819=DIRECTION('',(0.,-1.,0.));
#11820=DIRECTION('',(-0.5,0.,-0.866025403784439));
#11821=DIRECTION('center_axis',(-1.60246890531964E-16,0.,1.));
#11822=DIRECTION('ref_axis',(-1.,0.,-1.60246890531964E-16));
#11823=DIRECTION('',(1.,0.,1.60246890531964E-16));
#11824=DIRECTION('',(0.,-1.,0.));
#11825=DIRECTION('',(-1.,0.,-1.60246890531964E-16));
#11826=DIRECTION('center_axis',(0.866025403784439,0.,0.5));
#11827=DIRECTION('ref_axis',(-0.5,0.,0.866025403784439));
#11828=DIRECTION('',(0.5,0.,-0.866025403784439));
#11829=DIRECTION('',(-0.5,0.,0.866025403784439));
#11830=DIRECTION('center_axis',(0.,1.,0.));
#11831=DIRECTION('ref_axis',(1.,0.,0.));
#11832=DIRECTION('center_axis',(0.,-1.,0.));
#11833=DIRECTION('ref_axis',(0.,0.,-1.));
#11834=DIRECTION('center_axis',(0.,1.,0.));
#11835=DIRECTION('ref_axis',(1.,0.,0.));
#11836=DIRECTION('center_axis',(0.,1.,0.));
#11837=DIRECTION('ref_axis',(1.,0.,0.));
#11838=DIRECTION('center_axis',(0.,1.,0.));
#11839=DIRECTION('ref_axis',(0.,0.,1.));
#11840=DIRECTION('center_axis',(0.,-1.,0.));
#11841=DIRECTION('ref_axis',(1.,0.,0.));
#11842=DIRECTION('center_axis',(0.,-1.,0.));
#11843=DIRECTION('ref_axis',(1.,0.,0.));
#11844=DIRECTION('center_axis',(0.,-1.,0.));
#11845=DIRECTION('ref_axis',(1.,0.,0.));
#11846=DIRECTION('',(0.707106781186548,0.707106781186547,8.65956056235493E-17));
#11847=DIRECTION('center_axis',(0.,-1.,0.));
#11848=DIRECTION('ref_axis',(1.,0.,0.));
#11849=DIRECTION('center_axis',(0.,-1.,0.));
#11850=DIRECTION('ref_axis',(1.,0.,0.));
#11851=DIRECTION('',(0.,1.,0.));
#11852=DIRECTION('center_axis',(0.,1.,0.));
#11853=DIRECTION('ref_axis',(1.,0.,0.));
#11854=DIRECTION('center_axis',(0.,-1.,0.));
#11855=DIRECTION('ref_axis',(1.,0.,0.));
#11856=DIRECTION('',(-0.707106781186548,0.707106781186547,-8.65956056235494E-17));
#11857=DIRECTION('center_axis',(0.,-1.,0.));
#11858=DIRECTION('ref_axis',(0.,0.,-1.));
#11859=DIRECTION('center_axis',(0.,-1.,0.));
#11860=DIRECTION('ref_axis',(1.,0.,0.));
#11861=DIRECTION('center_axis',(0.,1.,0.));
#11862=DIRECTION('ref_axis',(1.,0.,0.));
#11863=DIRECTION('center_axis',(0.,1.,0.));
#11864=DIRECTION('ref_axis',(1.,0.,0.));
#11865=DIRECTION('',(-0.447213595499958,0.894427190999916,-5.47678698264203E-17));
#11866=DIRECTION('center_axis',(0.,-1.,0.));
#11867=DIRECTION('ref_axis',(1.,0.,0.));
#11868=DIRECTION('',(0.,1.,0.));
#15037=CARTESIAN_POINT('',(0.,0.,0.));
#15038=CARTESIAN_POINT('Origin',(0.173205080756888,-0.8,-0.3));
#15039=CARTESIAN_POINT('',(0.346410161513775,-0.8,0.));
#15040=CARTESIAN_POINT('',(0.173205080756888,-0.8,-0.3));
#15041=CARTESIAN_POINT('',(0.346410161513775,-0.8,0.));
#15042=CARTESIAN_POINT('',(0.173205080756888,-1.28,-0.3));
#15043=CARTESIAN_POINT('',(0.173205080756888,-0.8,-0.3));
#15044=CARTESIAN_POINT('',(0.346410161513775,-1.28,0.));
#15045=CARTESIAN_POINT('',(0.346410161513775,-1.28,0.));
#15046=CARTESIAN_POINT('',(0.346410161513775,-0.8,0.));
#15047=CARTESIAN_POINT('Origin',(-0.173205080756888,-0.8,-0.3));
#15048=CARTESIAN_POINT('',(-0.173205080756888,-0.8,-0.3));
#15049=CARTESIAN_POINT('',(0.173205080756888,-0.8,-0.3));
#15050=CARTESIAN_POINT('',(-0.173205080756888,-1.28,-0.3));
#15051=CARTESIAN_POINT('',(-0.173205080756888,-0.8,-0.3));
#15052=CARTESIAN_POINT('',(0.173205080756888,-1.28,-0.3));
#15053=CARTESIAN_POINT('Origin',(-0.346410161513775,-0.8,-5.55111512312578E-17));
#15054=CARTESIAN_POINT('',(-0.346410161513775,-0.8,-4.24230095489963E-17));
#15055=CARTESIAN_POINT('',(-0.173205080756888,-0.8,-0.3));
#15056=CARTESIAN_POINT('',(-0.346410161513775,-1.28,-5.55111512312578E-17));
#15057=CARTESIAN_POINT('',(-0.346410161513775,-0.8,-4.24230095489963E-17));
#15058=CARTESIAN_POINT('',(-0.173205080756888,-1.28,-0.3));
#15059=CARTESIAN_POINT('Origin',(-0.173205080756888,-0.8,0.3));
#15060=CARTESIAN_POINT('',(-0.173205080756888,-0.8,0.3));
#15061=CARTESIAN_POINT('',(-0.346410161513775,-0.8,-4.24230095489963E-17));
#15062=CARTESIAN_POINT('',(-0.173205080756888,-1.28,0.3));
#15063=CARTESIAN_POINT('',(-0.173205080756888,-0.8,0.3));
#15064=CARTESIAN_POINT('',(-0.346410161513775,-1.28,-4.24230095489963E-17));
#15065=CARTESIAN_POINT('Origin',(0.173205080756888,-0.8,0.3));
#15066=CARTESIAN_POINT('',(0.173205080756888,-0.8,0.3));
#15067=CARTESIAN_POINT('',(-0.173205080756888,-0.8,0.3));
#15068=CARTESIAN_POINT('',(0.173205080756888,-1.28,0.3));
#15069=CARTESIAN_POINT('',(0.173205080756888,-0.8,0.3));
#15070=CARTESIAN_POINT('',(-0.173205080756888,-1.28,0.3));
#15071=CARTESIAN_POINT('Origin',(0.346410161513775,-0.8,0.));
#15072=CARTESIAN_POINT('',(0.173205080756888,-0.8,0.3));
#15073=CARTESIAN_POINT('',(0.173205080756888,-1.28,0.3));
#15074=CARTESIAN_POINT('Origin',(0.,-0.8,-5.55111512312578E-17));
#15075=CARTESIAN_POINT('Origin',(0.,-1.28,-5.55111512312578E-17));
#15076=CARTESIAN_POINT('Origin',(0.,-2.5,0.));
#15077=CARTESIAN_POINT('',(-0.3933,-2.5,4.81653586104654E-17));
#15078=CARTESIAN_POINT('Origin',(0.,-2.5,0.));
#15079=CARTESIAN_POINT('Origin',(0.6,0.8,0.));
#15080=CARTESIAN_POINT('',(-0.6,0.8,-7.34788079488412E-17));
#15081=CARTESIAN_POINT('Origin',(0.,0.8,0.));
#15082=CARTESIAN_POINT('Origin',(0.,0.775,0.));
#15083=CARTESIAN_POINT('',(-0.65,0.75,-7.9602041944578E-17));
#15084=CARTESIAN_POINT('Origin',(0.,0.75,0.));
#15085=CARTESIAN_POINT('',(-0.625,0.775,-7.65404249467096E-17));
#15086=CARTESIAN_POINT('Origin',(0.,0.39,0.));
#15087=CARTESIAN_POINT('',(-0.65,0.0299999999999998,-7.9602041944578E-17));
#15088=CARTESIAN_POINT('Origin',(0.,0.0299999999999998,0.));
#15089=CARTESIAN_POINT('',(-0.65,0.39,-7.9602041944578E-17));
#15090=CARTESIAN_POINT('Origin',(0.,0.0150000000000001,0.));
#15091=CARTESIAN_POINT('',(-0.62,5.89805981832114E-17,-7.59281015471359E-17));
#15092=CARTESIAN_POINT('Origin',(0.,0.,0.));
#15093=CARTESIAN_POINT('',(-0.635,0.0150000000000001,-7.77650717458569E-17));
#15094=CARTESIAN_POINT('Origin',(0.42,0.,0.));
#15095=CARTESIAN_POINT('',(-0.42,-3.46944695195361E-18,-5.14351655641888E-17));
#15096=CARTESIAN_POINT('Origin',(0.,0.,0.));
#15097=CARTESIAN_POINT('Origin',(0.,-0.02,0.));
#15098=CARTESIAN_POINT('',(-0.3933,-0.0534000000000001,4.81653586104654E-17));
#15099=CARTESIAN_POINT('Origin',(0.,-0.0534000000000001,0.));
#15100=CARTESIAN_POINT('',(-0.41,-0.02,-5.02105187650415E-17));
#15101=CARTESIAN_POINT('Origin',(0.,-1.48,0.));
#15102=CARTESIAN_POINT('',(-0.3933,-1.48,-4.81653586104654E-17));
#17219=UNCERTAINTY_MEASURE_WITH_UNIT(LENGTH_MEASURE(0.001),#17323,
'DISTANCE_ACCURACY_VALUE',
'Maximum model space distance between geometric entities at asserted c
onnectivities');
#17261=UNCERTAINTY_MEASURE_WITH_UNIT(LENGTH_MEASURE(0.001),#17323,
'DISTANCE_ACCURACY_VALUE',
'Maximum model space distance between geometric entities at asserted c
onnectivities');
#17280=(
GEOMETRIC_REPRESENTATION_CONTEXT(3)
GLOBAL_UNCERTAINTY_ASSIGNED_CONTEXT((#17219))
GLOBAL_UNIT_ASSIGNED_CONTEXT((#17323,#17325,#17326))
REPRESENTATION_CONTEXT('','3D')
);
#17322=(
GEOMETRIC_REPRESENTATION_CONTEXT(3)
GLOBAL_UNCERTAINTY_ASSIGNED_CONTEXT((#17261))
GLOBAL_UNIT_ASSIGNED_CONTEXT((#17323,#17325,#17326))
REPRESENTATION_CONTEXT('','3D')
);
#17323=(
LENGTH_UNIT()
NAMED_UNIT(*)
SI_UNIT(.CENTI.,.METRE.)
);
#17325=(
NAMED_UNIT(*)
PLANE_ANGLE_UNIT()
SI_UNIT($,.RADIAN.)
);
#17326=(
NAMED_UNIT(*)
SI_UNIT($,.STERADIAN.)
SOLID_ANGLE_UNIT()
);
#17345=SHAPE_DEFINITION_REPRESENTATION(#17407,#17576);
#17407=PRODUCT_DEFINITION_SHAPE('',$,#17637);
#17576=SHAPE_REPRESENTATION('',(#10053),#17280);
#17618=PRODUCT_DEFINITION_CONTEXT('part definition',#17800,'design');
#17637=PRODUCT_DEFINITION('M8x25 Bolt','M8x25 Bolt',#17697,#17618);
#17697=PRODUCT_DEFINITION_FORMATION('',$,#17820);
#17800=APPLICATION_CONTEXT(
'Core Data for Automotive Mechanical Design Process');
#17801=PRODUCT_CONTEXT('part definition',#17800,'mechanical');
#17820=PRODUCT('M8x25 Bolt','M8x25 Bolt','M8x25 Bolt',(#17801));
#17932=COLOUR_RGB('Black',0.12,0.14,0.17);
#17933=FILL_AREA_STYLE_COLOUR('',#17932);
#17934=FILL_AREA_STYLE('',(#17933));
#17935=SURFACE_STYLE_FILL_AREA(#17934);
#17936=SURFACE_SIDE_STYLE('',(#17935));
#17937=SURFACE_STYLE_USAGE(.BOTH.,#17936);
#17938=PRESENTATION_STYLE_ASSIGNMENT((#17937));
ENDSEC;
END-ISO-10303-21;
